ISO-10303-21;
HEADER;
/* Generated by software containing ST-Developer
 * from STEP Tools, Inc. (www.steptools.com) 
 */

FILE_DESCRIPTION(
/* description */ ('Bin tilter linkage'),
/* implementation_level */ '2;1');

FILE_NAME(
/* name */ 'Bearing cap (5).step',
/* time_stamp */ '2026-10-28T03:26:24-07:00',
/* author */ (''),
/* organization */ (''),
/* preprocessor_version */ 'ST-DEVELOPER v20.2',
/* originating_system */ 'Autodesk Translation Framework v15.17.0.0',
/* authorisation */ '');

FILE_SCHEMA (('AUTOMOTIVE_DESIGN { 1 0 10303 214 3 1 1 }'));
ENDSEC;

DATA;
#10=MECHANICAL_DESIGN_GEOMETRIC_PRESENTATION_REPRESENTATION('',(#919),#23728);
#707=SHAPE_REPRESENTATION_RELATIONSHIP('SRR','None',#24173,#813);
#813=ADVANCED_BREP_SHAPE_REPRESENTATION('',(#1032),#23673);
#919=STYLED_ITEM('',(#24765),#1032);
#1032=MANIFOLD_SOLID_BREP('Body1',#12450);
#1344=FACE_BOUND('',#3352,.T.);
#1345=FACE_BOUND('',#3353,.T.);
#1346=FACE_BOUND('',#3354,.T.);
#1347=FACE_BOUND('',#3355,.T.);
#1348=FACE_BOUND('',#3356,.T.);
#1349=FACE_BOUND('',#3358,.T.);
#1350=FACE_BOUND('',#3359,.T.);
#1351=FACE_BOUND('',#3360,.T.);
#1352=FACE_BOUND('',#3361,.T.);
#1353=FACE_BOUND('',#3362,.T.);
#1695=PLANE('',#14609);
#1696=PLANE('',#14610);
#2311=FACE_OUTER_BOUND('',#3345,.T.);
#2312=FACE_OUTER_BOUND('',#3346,.T.);
#2313=FACE_OUTER_BOUND('',#3347,.T.);
#2314=FACE_OUTER_BOUND('',#3348,.T.);
#2315=FACE_OUTER_BOUND('',#3349,.T.);
#2316=FACE_OUTER_BOUND('',#3350,.T.);
#2317=FACE_OUTER_BOUND('',#3351,.T.);
#2318=FACE_OUTER_BOUND('',#3357,.T.);
#3345=EDGE_LOOP('',(#9961,#9962,#9963,#9964));
#3346=EDGE_LOOP('',(#9965,#9966,#9967,#9968));
#3347=EDGE_LOOP('',(#9969,#9970,#9971,#9972));
#3348=EDGE_LOOP('',(#9973,#9974,#9975,#9976));
#3349=EDGE_LOOP('',(#9977,#9978,#9979,#9980));
#3350=EDGE_LOOP('',(#9981,#9982,#9983,#9984));
#3351=EDGE_LOOP('',(#9985));
#3352=EDGE_LOOP('',(#9986));
#3353=EDGE_LOOP('',(#9987));
#3354=EDGE_LOOP('',(#9988));
#3355=EDGE_LOOP('',(#9989));
#3356=EDGE_LOOP('',(#9990));
#3357=EDGE_LOOP('',(#9991));
#3358=EDGE_LOOP('',(#9992));
#3359=EDGE_LOOP('',(#9993));
#3360=EDGE_LOOP('',(#9994));
#3361=EDGE_LOOP('',(#9995));
#3362=EDGE_LOOP('',(#9996));
#4211=LINE('',#21554,#4886);
#4212=LINE('',#21560,#4887);
#4213=LINE('',#21566,#4888);
#4214=LINE('',#21572,#4889);
#4215=LINE('',#21578,#4890);
#4216=LINE('',#21584,#4891);
#4886=VECTOR('',#17670,0.225000000000001);
#4887=VECTOR('',#17677,0.225000000000001);
#4888=VECTOR('',#17684,0.225000000000001);
#4889=VECTOR('',#17691,0.225000000000001);
#4890=VECTOR('',#17698,1.02);
#4891=VECTOR('',#17705,2.2);
#5631=CIRCLE('',#14592,0.225000000000001);
#5632=CIRCLE('',#14593,0.225000000000001);
#5633=CIRCLE('',#14595,0.225000000000001);
#5634=CIRCLE('',#14596,0.225000000000001);
#5635=CIRCLE('',#14598,0.225000000000001);
#5636=CIRCLE('',#14599,0.225000000000001);
#5637=CIRCLE('',#14601,0.225000000000001);
#5638=CIRCLE('',#14602,0.225000000000001);
#5639=CIRCLE('',#14604,1.02);
#5640=CIRCLE('',#14605,1.02);
#5641=CIRCLE('',#14607,2.2);
#5642=CIRCLE('',#14608,2.2);
#6485=VERTEX_POINT('',#21551);
#6486=VERTEX_POINT('',#21553);
#6487=VERTEX_POINT('',#21557);
#6488=VERTEX_POINT('',#21559);
#6489=VERTEX_POINT('',#21563);
#6490=VERTEX_POINT('',#21565);
#6491=VERTEX_POINT('',#21569);
#6492=VERTEX_POINT('',#21571);
#6493=VERTEX_POINT('',#21575);
#6494=VERTEX_POINT('',#21577);
#6495=VERTEX_POINT('',#21581);
#6496=VERTEX_POINT('',#21583);
#7720=EDGE_CURVE('',#6485,#6485,#5631,.T.);
#7721=EDGE_CURVE('',#6485,#6486,#4211,.T.);
#7722=EDGE_CURVE('',#6486,#6486,#5632,.T.);
#7723=EDGE_CURVE('',#6487,#6487,#5633,.T.);
#7724=EDGE_CURVE('',#6487,#6488,#4212,.T.);
#7725=EDGE_CURVE('',#6488,#6488,#5634,.T.);
#7726=EDGE_CURVE('',#6489,#6489,#5635,.T.);
#7727=EDGE_CURVE('',#6489,#6490,#4213,.T.);
#7728=EDGE_CURVE('',#6490,#6490,#5636,.T.);
#7729=EDGE_CURVE('',#6491,#6491,#5637,.T.);
#7730=EDGE_CURVE('',#6491,#6492,#4214,.T.);
#7731=EDGE_CURVE('',#6492,#6492,#5638,.T.);
#7732=EDGE_CURVE('',#6493,#6493,#5639,.T.);
#7733=EDGE_CURVE('',#6493,#6494,#4215,.T.);
#7734=EDGE_CURVE('',#6494,#6494,#5640,.T.);
#7735=EDGE_CURVE('',#6495,#6495,#5641,.T.);
#7736=EDGE_CURVE('',#6495,#6496,#4216,.T.);
#7737=EDGE_CURVE('',#6496,#6496,#5642,.T.);
#9961=ORIENTED_EDGE('',*,*,#7720,.F.);
#9962=ORIENTED_EDGE('',*,*,#7721,.T.);
#9963=ORIENTED_EDGE('',*,*,#7722,.F.);
#9964=ORIENTED_EDGE('',*,*,#7721,.F.);
#9965=ORIENTED_EDGE('',*,*,#7723,.F.);
#9966=ORIENTED_EDGE('',*,*,#7724,.T.);
#9967=ORIENTED_EDGE('',*,*,#7725,.F.);
#9968=ORIENTED_EDGE('',*,*,#7724,.F.);
#9969=ORIENTED_EDGE('',*,*,#7726,.F.);
#9970=ORIENTED_EDGE('',*,*,#7727,.T.);
#9971=ORIENTED_EDGE('',*,*,#7728,.F.);
#9972=ORIENTED_EDGE('',*,*,#7727,.F.);
#9973=ORIENTED_EDGE('',*,*,#7729,.F.);
#9974=ORIENTED_EDGE('',*,*,#7730,.T.);
#9975=ORIENTED_EDGE('',*,*,#7731,.F.);
#9976=ORIENTED_EDGE('',*,*,#7730,.F.);
#9977=ORIENTED_EDGE('',*,*,#7732,.F.);
#9978=ORIENTED_EDGE('',*,*,#7733,.T.);
#9979=ORIENTED_EDGE('',*,*,#7734,.T.);
#9980=ORIENTED_EDGE('',*,*,#7733,.F.);
#9981=ORIENTED_EDGE('',*,*,#7735,.F.);
#9982=ORIENTED_EDGE('',*,*,#7736,.T.);
#9983=ORIENTED_EDGE('',*,*,#7737,.T.);
#9984=ORIENTED_EDGE('',*,*,#7736,.F.);
#9985=ORIENTED_EDGE('',*,*,#7735,.T.);
#9986=ORIENTED_EDGE('',*,*,#7732,.T.);
#9987=ORIENTED_EDGE('',*,*,#7731,.T.);
#9988=ORIENTED_EDGE('',*,*,#7728,.T.);
#9989=ORIENTED_EDGE('',*,*,#7725,.T.);
#9990=ORIENTED_EDGE('',*,*,#7722,.T.);
#9991=ORIENTED_EDGE('',*,*,#7737,.F.);
#9992=ORIENTED_EDGE('',*,*,#7734,.F.);
#9993=ORIENTED_EDGE('',*,*,#7729,.T.);
#9994=ORIENTED_EDGE('',*,*,#7726,.T.);
#9995=ORIENTED_EDGE('',*,*,#7723,.T.);
#9996=ORIENTED_EDGE('',*,*,#7720,.T.);
#11481=CYLINDRICAL_SURFACE('',#14591,0.225000000000001);
#11482=CYLINDRICAL_SURFACE('',#14594,0.225000000000001);
#11483=CYLINDRICAL_SURFACE('',#14597,0.225000000000001);
#11484=CYLINDRICAL_SURFACE('',#14600,0.225000000000001);
#11485=CYLINDRICAL_SURFACE('',#14603,1.02);
#11486=CYLINDRICAL_SURFACE('',#14606,2.2);
#12036=ADVANCED_FACE('',(#2311),#11481,.F.);
#12037=ADVANCED_FACE('',(#2312),#11482,.F.);
#12038=ADVANCED_FACE('',(#2313),#11483,.F.);
#12039=ADVANCED_FACE('',(#2314),#11484,.F.);
#12040=ADVANCED_FACE('',(#2315),#11485,.F.);
#12041=ADVANCED_FACE('',(#2316),#11486,.T.);
#12042=ADVANCED_FACE('',(#2317,#1344,#1345,#1346,#1347,#1348),#1695,.T.);
#12043=ADVANCED_FACE('',(#2318,#1349,#1350,#1351,#1352,#1353),#1696,.F.);
#12450=CLOSED_SHELL('',(#12036,#12037,#12038,#12039,#12040,#12041,#12042,
#12043));
#14590=AXIS2_PLACEMENT_3D('',#21549,#17664,#17665);
#14591=AXIS2_PLACEMENT_3D('',#21550,#17666,#17667);
#14592=AXIS2_PLACEMENT_3D('',#21552,#17668,#17669);
#14593=AXIS2_PLACEMENT_3D('',#21555,#17671,#17672);
#14594=AXIS2_PLACEMENT_3D('',#21556,#17673,#17674);
#14595=AXIS2_PLACEMENT_3D('',#21558,#17675,#17676);
#14596=AXIS2_PLACEMENT_3D('',#21561,#17678,#17679);
#14597=AXIS2_PLACEMENT_3D('',#21562,#17680,#17681);
#14598=AXIS2_PLACEMENT_3D('',#21564,#17682,#17683);
#14599=AXIS2_PLACEMENT_3D('',#21567,#17685,#17686);
#14600=AXIS2_PLACEMENT_3D('',#21568,#17687,#17688);
#14601=AXIS2_PLACEMENT_3D('',#21570,#17689,#17690);
#14602=AXIS2_PLACEMENT_3D('',#21573,#17692,#17693);
#14603=AXIS2_PLACEMENT_3D('',#21574,#17694,#17695);
#14604=AXIS2_PLACEMENT_3D('',#21576,#17696,#17697);
#14605=AXIS2_PLACEMENT_3D('',#21579,#17699,#17700);
#14606=AXIS2_PLACEMENT_3D('',#21580,#17701,#17702);
#14607=AXIS2_PLACEMENT_3D('',#21582,#17703,#17704);
#14608=AXIS2_PLACEMENT_3D('',#21585,#17706,#17707);
#14609=AXIS2_PLACEMENT_3D('',#21586,#17708,#17709);
#14610=AXIS2_PLACEMENT_3D('',#21587,#17710,#17711);
#17664=DIRECTION('axis',(0.,0.,1.));
#17665=DIRECTION('refdir',(1.,0.,0.));
#17666=DIRECTION('center_axis',(0.,1.,0.));
#17667=DIRECTION('ref_axis',(1.,0.,0.));
#17668=DIRECTION('center_axis',(0.,1.,0.));
#17669=DIRECTION('ref_axis',(1.,0.,0.));
#17670=DIRECTION('',(0.,1.,0.));
#17671=DIRECTION('center_axis',(0.,-1.,0.));
#17672=DIRECTION('ref_axis',(1.,0.,0.));
#17673=DIRECTION('center_axis',(0.,1.,0.));
#17674=DIRECTION('ref_axis',(1.,0.,0.));
#17675=DIRECTION('center_axis',(0.,1.,0.));
#17676=DIRECTION('ref_axis',(1.,0.,0.));
#17677=DIRECTION('',(0.,1.,0.));
#17678=DIRECTION('center_axis',(0.,-1.,0.));
#17679=DIRECTION('ref_axis',(1.,0.,0.));
#17680=DIRECTION('center_axis',(0.,1.,0.));
#17681=DIRECTION('ref_axis',(1.,0.,0.));
#17682=DIRECTION('center_axis',(0.,1.,0.));
#17683=DIRECTION('ref_axis',(1.,0.,0.));
#17684=DIRECTION('',(0.,1.,0.));
#17685=DIRECTION('center_axis',(0.,-1.,0.));
#17686=DIRECTION('ref_axis',(1.,0.,0.));
#17687=DIRECTION('center_axis',(0.,1.,0.));
#17688=DIRECTION('ref_axis',(1.,0.,0.));
#17689=DIRECTION('center_axis',(0.,1.,0.));
#17690=DIRECTION('ref_axis',(1.,0.,0.));
#17691=DIRECTION('',(0.,1.,0.));
#17692=DIRECTION('center_axis',(0.,-1.,0.));
#17693=DIRECTION('ref_axis',(1.,0.,0.));
#17694=DIRECTION('center_axis',(0.,1.,0.));
#17695=DIRECTION('ref_axis',(1.,0.,0.));
#17696=DIRECTION('center_axis',(0.,-1.,0.));
#17697=DIRECTION('ref_axis',(1.,0.,0.));
#17698=DIRECTION('',(0.,-1.,0.));
#17699=DIRECTION('center_axis',(0.,-1.,0.));
#17700=DIRECTION('ref_axis',(1.,0.,0.));
#17701=DIRECTION('center_axis',(0.,1.,0.));
#17702=DIRECTION('ref_axis',(1.,0.,0.));
#17703=DIRECTION('center_axis',(0.,1.,0.));
#17704=DIRECTION('ref_axis',(1.,0.,0.));
#17705=DIRECTION('',(0.,-1.,0.));
#17706=DIRECTION('center_axis',(0.,1.,0.));
#17707=DIRECTION('ref_axis',(1.,0.,0.));
#17708=DIRECTION('center_axis',(0.,1.,0.));
#17709=DIRECTION('ref_axis',(1.,0.,0.));
#17710=DIRECTION('center_axis',(0.,1.,0.));
#17711=DIRECTION('ref_axis',(1.,0.,0.));
#21549=CARTESIAN_POINT('',(0.,0.,0.));
#21550=CARTESIAN_POINT('Origin',(16.6918524548049,0.4,13.6918524548049));
#21551=CARTESIAN_POINT('',(16.4668524548049,0.5,13.6918524548049));
#21552=CARTESIAN_POINT('Origin',(16.6918524548049,0.5,13.6918524548049));
#21553=CARTESIAN_POINT('',(16.4668524548049,0.8,13.6918524548049));
#21554=CARTESIAN_POINT('',(16.4668524548049,0.4,13.6918524548049));
#21555=CARTESIAN_POINT('Origin',(16.6918524548049,0.8,13.6918524548049));
#21556=CARTESIAN_POINT('Origin',(16.6918524548049,0.4,16.3081475451951));
#21557=CARTESIAN_POINT('',(16.4668524548049,0.5,16.3081475451951));
#21558=CARTESIAN_POINT('Origin',(16.6918524548049,0.5,16.3081475451951));
#21559=CARTESIAN_POINT('',(16.4668524548049,0.8,16.3081475451951));
#21560=CARTESIAN_POINT('',(16.4668524548049,0.4,16.3081475451951));
#21561=CARTESIAN_POINT('Origin',(16.6918524548049,0.8,16.3081475451951));
#21562=CARTESIAN_POINT('Origin',(19.3081475451951,0.4,16.3081475451951));
#21563=CARTESIAN_POINT('',(19.0831475451951,0.5,16.3081475451951));
#21564=CARTESIAN_POINT('Origin',(19.3081475451951,0.5,16.3081475451951));
#21565=CARTESIAN_POINT('',(19.0831475451951,0.8,16.3081475451951));
#21566=CARTESIAN_POINT('',(19.0831475451951,0.4,16.3081475451951));
#21567=CARTESIAN_POINT('Origin',(19.3081475451951,0.8,16.3081475451951));
#21568=CARTESIAN_POINT('Origin',(19.3081475451951,0.4,13.6918524548049));
#21569=CARTESIAN_POINT('',(19.0831475451951,0.5,13.6918524548049));
#21570=CARTESIAN_POINT('Origin',(19.3081475451951,0.5,13.6918524548049));
#21571=CARTESIAN_POINT('',(19.0831475451951,0.8,13.6918524548049));
#21572=CARTESIAN_POINT('',(19.0831475451951,0.4,13.6918524548049));
#21573=CARTESIAN_POINT('Origin',(19.3081475451951,0.8,13.6918524548049));
#21574=CARTESIAN_POINT('Origin',(18.,0.5,15.));
#21575=CARTESIAN_POINT('',(16.98,0.8,15.));
#21576=CARTESIAN_POINT('Origin',(18.,0.8,15.));
#21577=CARTESIAN_POINT('',(16.98,0.5,15.));
#21578=CARTESIAN_POINT('',(16.98,0.5,15.));
#21579=CARTESIAN_POINT('Origin',(18.,0.5,15.));
#21580=CARTESIAN_POINT('Origin',(18.,0.5,15.));
#21581=CARTESIAN_POINT('',(15.8,0.8,15.));
#21582=CARTESIAN_POINT('Origin',(18.,0.8,15.));
#21583=CARTESIAN_POINT('',(15.8,0.5,15.));
#21584=CARTESIAN_POINT('',(15.8,0.5,15.));
#21585=CARTESIAN_POINT('Origin',(18.,0.5,15.));
#21586=CARTESIAN_POINT('Origin',(18.,0.8,15.));
#21587=CARTESIAN_POINT('Origin',(18.,0.5,15.));
#23556=UNCERTAINTY_MEASURE_WITH_UNIT(LENGTH_MEASURE(0.001),#23729,
'DISTANCE_ACCURACY_VALUE',
'Maximum model space distance between geometric entities at asserted c
onnectivities');
#23611=UNCERTAINTY_MEASURE_WITH_UNIT(LENGTH_MEASURE(0.001),#23729,
'DISTANCE_ACCURACY_VALUE',
'Maximum model space distance between geometric entities at asserted c
onnectivities');
#23673=(
GEOMETRIC_REPRESENTATION_CONTEXT(3)
GLOBAL_UNCERTAINTY_ASSIGNED_CONTEXT((#23556))
GLOBAL_UNIT_ASSIGNED_CONTEXT((#23729,#23731,#23732))
REPRESENTATION_CONTEXT('','3D')
);
#23728=(
GEOMETRIC_REPRESENTATION_CONTEXT(3)
GLOBAL_UNCERTAINTY_ASSIGNED_CONTEXT((#23611))
GLOBAL_UNIT_ASSIGNED_CONTEXT((#23729,#23731,#23732))
REPRESENTATION_CONTEXT('','3D')
);
#23729=(
LENGTH_UNIT()
NAMED_UNIT(*)
SI_UNIT(.CENTI.,.METRE.)
);
#23731=(
NAMED_UNIT(*)
PLANE_ANGLE_UNIT()
SI_UNIT($,.RADIAN.)
);
#23732=(
NAMED_UNIT(*)
SI_UNIT($,.STERADIAN.)
SOLID_ANGLE_UNIT()
);
#23794=SHAPE_DEFINITION_REPRESENTATION(#23910,#24173);
#23910=PRODUCT_DEFINITION_SHAPE('',$,#24290);
#24173=SHAPE_REPRESENTATION('',(#14590),#23673);
#24228=PRODUCT_DEFINITION_CONTEXT('part definition',#24578,'design');
#24290=PRODUCT_DEFINITION('Bearing cap (5)','Bearing cap (5)',#24406,#24228);
#24406=PRODUCT_DEFINITION_FORMATION('',$,#24641);
#24578=APPLICATION_CONTEXT(
'Core Data for Automotive Mechanical Design Process');
#24579=PRODUCT_CONTEXT('part definition',#24578,'mechanical');
#24641=PRODUCT('Bearing cap (5)','Bearing cap (5)','Bearing cap (5)',(#24579));
#24759=COLOUR_RGB('Grey',0.48,0.52,0.57);
#24760=FILL_AREA_STYLE_COLOUR('',#24759);
#24761=FILL_AREA_STYLE('',(#24760));
#24762=SURFACE_STYLE_FILL_AREA(#24761);
#24763=SURFACE_SIDE_STYLE('',(#24762));
#24764=SURFACE_STYLE_USAGE(.BOTH.,#24763);
#24765=PRESENTATION_STYLE_ASSIGNMENT((#24764));
ENDSEC;
END-ISO-10303-21;
